ISO-10303-21;
HEADER;
/* Generated by software containing ST-Developer
 * from STEP Tools, Inc. (www.steptools.com) 
 */

FILE_DESCRIPTION(
/* description */ ('PAT-072'),
/* implementation_level */ '2;1');

FILE_NAME(
/* name */ 'Outlet tube (2).step',
/* time_stamp */ '2026-10-29T20:11:56-07:00',
/* author */ (''),
/* organization */ (''),
/* preprocessor_version */ 'ST-DEVELOPER v20.2',
/* originating_system */ 'Autodesk Translation Framework v15.17.0.0',
/* authorisation */ '');

FILE_SCHEMA (('AUTOMOTIVE_DESIGN { 1 0 10303 214 3 1 1 }'));
ENDSEC;

DATA;
#10=MECHANICAL_DESIGN_GEOMETRIC_PRESENTATION_REPRESENTATION('',(#342),#11432);
#270=SHAPE_REPRESENTATION_RELATIONSHIP('SRR','None',#11574,#306);
#306=ADVANCED_BREP_SHAPE_REPRESENTATION('',(#378),#11405);
#342=STYLED_ITEM('',(#11812),#378);
#378=MANIFOLD_SOLID_BREP('Body1',#6077);
#472=FACE_BOUND('',#1368,.T.);
#473=FACE_BOUND('',#1370,.T.);
#637=PLANE('',#6763);
#638=PLANE('',#6764);
#923=FACE_OUTER_BOUND('',#1365,.T.);
#924=FACE_OUTER_BOUND('',#1366,.T.);
#925=FACE_OUTER_BOUND('',#1367,.T.);
#926=FACE_OUTER_BOUND('',#1369,.T.);
#1365=EDGE_LOOP('',(#4582,#4583,#4584,#4585));
#1366=EDGE_LOOP('',(#4586,#4587,#4588,#4589));
#1367=EDGE_LOOP('',(#4590));
#1368=EDGE_LOOP('',(#4591));
#1369=EDGE_LOOP('',(#4592));
#1370=EDGE_LOOP('',(#4593));
#1824=LINE('',#10099,#2243);
#1825=LINE('',#10105,#2244);
#2243=VECTOR('',#7889,0.2);
#2244=VECTOR('',#7896,0.3);
#2655=CIRCLE('',#6758,0.2);
#2656=CIRCLE('',#6759,0.2);
#2657=CIRCLE('',#6761,0.3);
#2658=CIRCLE('',#6762,0.3);
#3004=VERTEX_POINT('',#10096);
#3005=VERTEX_POINT('',#10098);
#3006=VERTEX_POINT('',#10102);
#3007=VERTEX_POINT('',#10104);
#3580=EDGE_CURVE('',#3004,#3004,#2655,.T.);
#3581=EDGE_CURVE('',#3004,#3005,#1824,.T.);
#3582=EDGE_CURVE('',#3005,#3005,#2656,.T.);
#3583=EDGE_CURVE('',#3006,#3006,#2657,.T.);
#3584=EDGE_CURVE('',#3006,#3007,#1825,.T.);
#3585=EDGE_CURVE('',#3007,#3007,#2658,.T.);
#4582=ORIENTED_EDGE('',*,*,#3580,.F.);
#4583=ORIENTED_EDGE('',*,*,#3581,.T.);
#4584=ORIENTED_EDGE('',*,*,#3582,.T.);
#4585=ORIENTED_EDGE('',*,*,#3581,.F.);
#4586=ORIENTED_EDGE('',*,*,#3583,.F.);
#4587=ORIENTED_EDGE('',*,*,#3584,.T.);
#4588=ORIENTED_EDGE('',*,*,#3585,.T.);
#4589=ORIENTED_EDGE('',*,*,#3584,.F.);
#4590=ORIENTED_EDGE('',*,*,#3583,.T.);
#4591=ORIENTED_EDGE('',*,*,#3580,.T.);
#4592=ORIENTED_EDGE('',*,*,#3585,.F.);
#4593=ORIENTED_EDGE('',*,*,#3582,.F.);
#5618=CYLINDRICAL_SURFACE('',#6757,0.2);
#5619=CYLINDRICAL_SURFACE('',#6760,0.3);
#5822=ADVANCED_FACE('',(#923),#5618,.F.);
#5823=ADVANCED_FACE('',(#924),#5619,.T.);
#5824=ADVANCED_FACE('',(#925,#472),#637,.T.);
#5825=ADVANCED_FACE('',(#926,#473),#638,.F.);
#6077=CLOSED_SHELL('',(#5822,#5823,#5824,#5825));
#6756=AXIS2_PLACEMENT_3D('',#10094,#7883,#7884);
#6757=AXIS2_PLACEMENT_3D('',#10095,#7885,#7886);
#6758=AXIS2_PLACEMENT_3D('',#10097,#7887,#7888);
#6759=AXIS2_PLACEMENT_3D('',#10100,#7890,#7891);
#6760=AXIS2_PLACEMENT_3D('',#10101,#7892,#7893);
#6761=AXIS2_PLACEMENT_3D('',#10103,#7894,#7895);
#6762=AXIS2_PLACEMENT_3D('',#10106,#7897,#7898);
#6763=AXIS2_PLACEMENT_3D('',#10107,#7899,#7900);
#6764=AXIS2_PLACEMENT_3D('',#10108,#7901,#7902);
#7883=DIRECTION('axis',(0.,0.,1.));
#7884=DIRECTION('refdir',(1.,0.,0.));
#7885=DIRECTION('center_axis',(0.,1.,0.));
#7886=DIRECTION('ref_axis',(1.,0.,0.));
#7887=DIRECTION('center_axis',(0.,-1.,0.));
#7888=DIRECTION('ref_axis',(1.,0.,0.));
#7889=DIRECTION('',(0.,-1.,0.));
#7890=DIRECTION('center_axis',(0.,-1.,0.));
#7891=DIRECTION('ref_axis',(1.,0.,0.));
#7892=DIRECTION('center_axis',(0.,1.,0.));
#7893=DIRECTION('ref_axis',(1.,0.,0.));
#7894=DIRECTION('center_axis',(0.,1.,0.));
#7895=DIRECTION('ref_axis',(1.,0.,0.));
#7896=DIRECTION('',(0.,-1.,0.));
#7897=DIRECTION('center_axis',(0.,1.,0.));
#7898=DIRECTION('ref_axis',(1.,0.,0.));
#7899=DIRECTION('center_axis',(0.,1.,0.));
#7900=DIRECTION('ref_axis',(1.,0.,0.));
#7901=DIRECTION('center_axis',(0.,1.,0.));
#7902=DIRECTION('ref_axis',(1.,0.,0.));
#10094=CARTESIAN_POINT('',(0.,0.,0.));
#10095=CARTESIAN_POINT('Origin',(1.25,-6.5,4.));
#10096=CARTESIAN_POINT('',(1.05,-3.2,4.));
#10097=CARTESIAN_POINT('Origin',(1.25,-3.2,4.));
#10098=CARTESIAN_POINT('',(1.05,-6.5,4.));
#10099=CARTESIAN_POINT('',(1.05,-6.5,4.));
#10100=CARTESIAN_POINT('Origin',(1.25,-6.5,4.));
#10101=CARTESIAN_POINT('Origin',(1.25,-6.5,4.));
#10102=CARTESIAN_POINT('',(0.95,-3.2,4.));
#10103=CARTESIAN_POINT('Origin',(1.25,-3.2,4.));
#10104=CARTESIAN_POINT('',(0.95,-6.5,4.));
#10105=CARTESIAN_POINT('',(0.95,-6.5,4.));
#10106=CARTESIAN_POINT('Origin',(1.25,-6.5,4.));
#10107=CARTESIAN_POINT('Origin',(1.25,-3.2,4.));
#10108=CARTESIAN_POINT('Origin',(1.25,-6.5,4.));
#11366=UNCERTAINTY_MEASURE_WITH_UNIT(LENGTH_MEASURE(0.001),#11433,
'DISTANCE_ACCURACY_VALUE',
'Maximum model space distance between geometric entities at asserted c
onnectivities');
#11393=UNCERTAINTY_MEASURE_WITH_UNIT(LENGTH_MEASURE(0.001),#11433,
'DISTANCE_ACCURACY_VALUE',
'Maximum model space distance between geometric entities at asserted c
onnectivities');
#11405=(
GEOMETRIC_REPRESENTATION_CONTEXT(3)
GLOBAL_UNCERTAINTY_ASSIGNED_CONTEXT((#11366))
GLOBAL_UNIT_ASSIGNED_CONTEXT((#11433,#11435,#11436))
REPRESENTATION_CONTEXT('','3D')
);
#11432=(
GEOMETRIC_REPRESENTATION_CONTEXT(3)
GLOBAL_UNCERTAINTY_ASSIGNED_CONTEXT((#11393))
GLOBAL_UNIT_ASSIGNED_CONTEXT((#11433,#11435,#11436))
REPRESENTATION_CONTEXT('','3D')
);
#11433=(
LENGTH_UNIT()
NAMED_UNIT(*)
SI_UNIT(.CENTI.,.METRE.)
);
#11435=(
NAMED_UNIT(*)
PLANE_ANGLE_UNIT()
SI_UNIT($,.RADIAN.)
);
#11436=(
NAMED_UNIT(*)
SI_UNIT($,.STERADIAN.)
SOLID_ANGLE_UNIT()
);
#11448=SHAPE_DEFINITION_REPRESENTATION(#11486,#11574);
#11486=PRODUCT_DEFINITION_SHAPE('',$,#11613);
#11574=SHAPE_REPRESENTATION('',(#6756),#11405);
#11601=PRODUCT_DEFINITION_CONTEXT('part definition',#11717,'design');
#11613=PRODUCT_DEFINITION('Outlet tube (2)','Outlet tube (2)',
#11651,#11601);
#11651=PRODUCT_DEFINITION_FORMATION('',$,#11730);
#11717=APPLICATION_CONTEXT(
'Core Data for Automotive Mechanical Design Process');
#11718=PRODUCT_CONTEXT('part definition',#11717,'mechanical');
#11730=PRODUCT('Outlet tube (2)','Outlet tube (2)',
'Outlet tube (2)',(#11718));
#11806=COLOUR_RGB('Sky Blue',0.24,0.69,0.87);
#11807=FILL_AREA_STYLE_COLOUR('',#11806);
#11808=FILL_AREA_STYLE('',(#11807));
#11809=SURFACE_STYLE_FILL_AREA(#11808);
#11810=SURFACE_SIDE_STYLE('',(#11809));
#11811=SURFACE_STYLE_USAGE(.BOTH.,#11810);
#11812=PRESENTATION_STYLE_ASSIGNMENT((#11811));
ENDSEC;
END-ISO-10303-21;
